ISO-10303-21;
HEADER;
/* Generated by software containing ST-Developer
 * from STEP Tools, Inc. (www.steptools.com) 
 */

FILE_DESCRIPTION(
/* description */ ('Flywheel Crank-Slider'),
/* implementation_level */ '2;1');

FILE_NAME(
/* name */ 'Rod bearing retainer (3).step',
/* time_stamp */ '2026-10-28T03:23:13-07:00',
/* author */ (''),
/* organization */ (''),
/* preprocessor_version */ 'ST-DEVELOPER v20.2',
/* originating_system */ 'Autodesk Translation Framework v15.17.0.0',
/* authorisation */ '');

FILE_SCHEMA (('AUTOMOTIVE_DESIGN { 1 0 10303 214 3 1 1 }'));
ENDSEC;

DATA;
#10=MECHANICAL_DESIGN_GEOMETRIC_PRESENTATION_REPRESENTATION('',(#705),#17322);
#600=SHAPE_REPRESENTATION_RELATIONSHIP('SRR','None',#17599,#652);
#652=ADVANCED_BREP_SHAPE_REPRESENTATION('',(#762),#17303);
#705=STYLED_ITEM('',(#17931),#762);
#762=MANIFOLD_SOLID_BREP('Body1',#9087);
#941=FACE_BOUND('',#2392,.T.);
#942=FACE_BOUND('',#2394,.T.);
#1240=PLANE('',#10391);
#1241=PLANE('',#10392);
#1698=FACE_OUTER_BOUND('',#2389,.T.);
#1699=FACE_OUTER_BOUND('',#2390,.T.);
#1700=FACE_OUTER_BOUND('',#2391,.T.);
#1701=FACE_OUTER_BOUND('',#2393,.T.);
#2389=EDGE_LOOP('',(#7686,#7687,#7688,#7689));
#2390=EDGE_LOOP('',(#7690,#7691,#7692,#7693));
#2391=EDGE_LOOP('',(#7694));
#2392=EDGE_LOOP('',(#7695));
#2393=EDGE_LOOP('',(#7696));
#2394=EDGE_LOOP('',(#7697));
#3084=LINE('',#16038,#3695);
#3085=LINE('',#16044,#3696);
#3695=VECTOR('',#12702,1.1);
#3696=VECTOR('',#12709,2.);
#4116=CIRCLE('',#10386,1.1);
#4117=CIRCLE('',#10387,1.1);
#4118=CIRCLE('',#10389,2.);
#4119=CIRCLE('',#10390,2.);
#4795=VERTEX_POINT('',#16035);
#4796=VERTEX_POINT('',#16037);
#4797=VERTEX_POINT('',#16041);
#4798=VERTEX_POINT('',#16043);
#5800=EDGE_CURVE('',#4795,#4795,#4116,.T.);
#5801=EDGE_CURVE('',#4795,#4796,#3084,.T.);
#5802=EDGE_CURVE('',#4796,#4796,#4117,.T.);
#5803=EDGE_CURVE('',#4797,#4797,#4118,.T.);
#5804=EDGE_CURVE('',#4797,#4798,#3085,.T.);
#5805=EDGE_CURVE('',#4798,#4798,#4119,.T.);
#7686=ORIENTED_EDGE('',*,*,#5800,.F.);
#7687=ORIENTED_EDGE('',*,*,#5801,.T.);
#7688=ORIENTED_EDGE('',*,*,#5802,.T.);
#7689=ORIENTED_EDGE('',*,*,#5801,.F.);
#7690=ORIENTED_EDGE('',*,*,#5803,.F.);
#7691=ORIENTED_EDGE('',*,*,#5804,.T.);
#7692=ORIENTED_EDGE('',*,*,#5805,.T.);
#7693=ORIENTED_EDGE('',*,*,#5804,.F.);
#7694=ORIENTED_EDGE('',*,*,#5803,.T.);
#7695=ORIENTED_EDGE('',*,*,#5800,.T.);
#7696=ORIENTED_EDGE('',*,*,#5805,.F.);
#7697=ORIENTED_EDGE('',*,*,#5802,.F.);
#8459=CYLINDRICAL_SURFACE('',#10385,1.1);
#8460=CYLINDRICAL_SURFACE('',#10388,2.);
#8889=ADVANCED_FACE('',(#1698),#8459,.F.);
#8890=ADVANCED_FACE('',(#1699),#8460,.T.);
#8891=ADVANCED_FACE('',(#1700,#941),#1240,.T.);
#8892=ADVANCED_FACE('',(#1701,#942),#1241,.F.);
#9087=CLOSED_SHELL('',(#8889,#8890,#8891,#8892));
#10384=AXIS2_PLACEMENT_3D('',#16033,#12696,#12697);
#10385=AXIS2_PLACEMENT_3D('',#16034,#12698,#12699);
#10386=AXIS2_PLACEMENT_3D('',#16036,#12700,#12701);
#10387=AXIS2_PLACEMENT_3D('',#16039,#12703,#12704);
#10388=AXIS2_PLACEMENT_3D('',#16040,#12705,#12706);
#10389=AXIS2_PLACEMENT_3D('',#16042,#12707,#12708);
#10390=AXIS2_PLACEMENT_3D('',#16045,#12710,#12711);
#10391=AXIS2_PLACEMENT_3D('',#16046,#12712,#12713);
#10392=AXIS2_PLACEMENT_3D('',#16047,#12714,#12715);
#12696=DIRECTION('axis',(0.,0.,1.));
#12697=DIRECTION('refdir',(1.,0.,0.));
#12698=DIRECTION('center_axis',(0.,1.,0.));
#12699=DIRECTION('ref_axis',(1.,0.,0.));
#12700=DIRECTION('center_axis',(0.,-1.,0.));
#12701=DIRECTION('ref_axis',(1.,0.,0.));
#12702=DIRECTION('',(0.,-1.,0.));
#12703=DIRECTION('center_axis',(0.,-1.,0.));
#12704=DIRECTION('ref_axis',(1.,0.,0.));
#12705=DIRECTION('center_axis',(0.,1.,0.));
#12706=DIRECTION('ref_axis',(1.,0.,0.));
#12707=DIRECTION('center_axis',(0.,1.,0.));
#12708=DIRECTION('ref_axis',(1.,0.,0.));
#12709=DIRECTION('',(0.,-1.,0.));
#12710=DIRECTION('center_axis',(0.,1.,0.));
#12711=DIRECTION('ref_axis',(1.,0.,0.));
#12712=DIRECTION('center_axis',(0.,1.,0.));
#12713=DIRECTION('ref_axis',(1.,0.,0.));
#12714=DIRECTION('center_axis',(0.,1.,0.));
#12715=DIRECTION('ref_axis',(1.,0.,0.));
#16033=CARTESIAN_POINT('',(0.,0.,0.));
#16034=CARTESIAN_POINT('Origin',(12.,3.4,10.));
#16035=CARTESIAN_POINT('',(10.9,3.6,10.));
#16036=CARTESIAN_POINT('Origin',(12.,3.6,10.));
#16037=CARTESIAN_POINT('',(10.9,3.4,10.));
#16038=CARTESIAN_POINT('',(10.9,3.4,10.));
#16039=CARTESIAN_POINT('Origin',(12.,3.4,10.));
#16040=CARTESIAN_POINT('Origin',(12.,3.4,10.));
#16041=CARTESIAN_POINT('',(10.,3.6,10.));
#16042=CARTESIAN_POINT('Origin',(12.,3.6,10.));
#16043=CARTESIAN_POINT('',(10.,3.4,10.));
#16044=CARTESIAN_POINT('',(10.,3.4,10.));
#16045=CARTESIAN_POINT('Origin',(12.,3.4,10.));
#16046=CARTESIAN_POINT('Origin',(12.,3.6,10.));
#16047=CARTESIAN_POINT('Origin',(12.,3.4,10.));
#17242=UNCERTAINTY_MEASURE_WITH_UNIT(LENGTH_MEASURE(0.001),#17323,
'DISTANCE_ACCURACY_VALUE',
'Maximum model space distance between geometric entities at asserted c
onnectivities');
#17261=UNCERTAINTY_MEASURE_WITH_UNIT(LENGTH_MEASURE(0.001),#17323,
'DISTANCE_ACCURACY_VALUE',
'Maximum model space distance between geometric entities at asserted c
onnectivities');
#17303=(
GEOMETRIC_REPRESENTATION_CONTEXT(3)
GLOBAL_UNCERTAINTY_ASSIGNED_CONTEXT((#17242))
GLOBAL_UNIT_ASSIGNED_CONTEXT((#17323,#17325,#17326))
REPRESENTATION_CONTEXT('','3D')
);
#17322=(
GEOMETRIC_REPRESENTATION_CONTEXT(3)
GLOBAL_UNCERTAINTY_ASSIGNED_CONTEXT((#17261))
GLOBAL_UNIT_ASSIGNED_CONTEXT((#17323,#17325,#17326))
REPRESENTATION_CONTEXT('','3D')
);
#17323=(
LENGTH_UNIT()
NAMED_UNIT(*)
SI_UNIT(.CENTI.,.METRE.)
);
#17325=(
NAMED_UNIT(*)
PLANE_ANGLE_UNIT()
SI_UNIT($,.RADIAN.)
);
#17326=(
NAMED_UNIT(*)
SI_UNIT($,.STERADIAN.)
SOLID_ANGLE_UNIT()
);
#17368=SHAPE_DEFINITION_REPRESENTATION(#17430,#17599);
#17430=PRODUCT_DEFINITION_SHAPE('',$,#17660);
#17599=SHAPE_REPRESENTATION('',(#10384),#17303);
#17618=PRODUCT_DEFINITION_CONTEXT('part definition',#17800,'design');
#17660=PRODUCT_DEFINITION('Rod bearing retainer (3)',
'Rod bearing retainer (3)',#17720,#17618);
#17720=PRODUCT_DEFINITION_FORMATION('',$,#17843);
#17800=APPLICATION_CONTEXT(
'Core Data for Automotive Mechanical Design Process');
#17801=PRODUCT_CONTEXT('part definition',#17800,'mechanical');
#17843=PRODUCT('Rod bearing retainer (3)','Rod bearing retainer (3)',
'Rod bearing retainer (3)',(#17801));
#17925=COLOUR_RGB('Grey',0.48,0.52,0.57);
#17926=FILL_AREA_STYLE_COLOUR('',#17925);
#17927=FILL_AREA_STYLE('',(#17926));
#17928=SURFACE_STYLE_FILL_AREA(#17927);
#17929=SURFACE_SIDE_STYLE('',(#17928));
#17930=SURFACE_STYLE_USAGE(.BOTH.,#17929);
#17931=PRESENTATION_STYLE_ASSIGNMENT((#17930));
ENDSEC;
END-ISO-10303-21;
